ISO-10303-21;
HEADER;
/* Generated by software containing ST-Developer
 * from STEP Tools, Inc. (www.steptools.com) 
 */

FILE_DESCRIPTION(
/* description */ ('Line shaft on three pillow blocks'),
/* implementation_level */ '2;1');

FILE_NAME(
/* name */ 'Mounting reducer bush (5).step',
/* time_stamp */ '2026-10-27T10:49:19-07:00',
/* author */ (''),
/* organization */ (''),
/* preprocessor_version */ 'ST-DEVELOPER v20.2',
/* originating_system */ 'Autodesk Translation Framework v15.17.0.0',
/* authorisation */ '');

FILE_SCHEMA (('AUTOMOTIVE_DESIGN { 1 0 10303 214 3 1 1 }'));
ENDSEC;

DATA;
#10=MECHANICAL_DESIGN_GEOMETRIC_PRESENTATION_REPRESENTATION('',(#348),#8377);
#294=SHAPE_REPRESENTATION_RELATIONSHIP('SRR','None',#8509,#321);
#321=ADVANCED_BREP_SHAPE_REPRESENTATION('',(#376),#8358);
#348=STYLED_ITEM('',(#8732),#376);
#376=MANIFOLD_SOLID_BREP('Body1',#4334);
#425=FACE_BOUND('',#1011,.T.);
#426=FACE_BOUND('',#1013,.T.);
#532=PLANE('',#4788);
#533=PLANE('',#4789);
#722=FACE_OUTER_BOUND('',#1008,.T.);
#723=FACE_OUTER_BOUND('',#1009,.T.);
#724=FACE_OUTER_BOUND('',#1010,.T.);
#725=FACE_OUTER_BOUND('',#1012,.T.);
#1008=EDGE_LOOP('',(#3213,#3214,#3215,#3216));
#1009=EDGE_LOOP('',(#3217,#3218,#3219,#3220));
#1010=EDGE_LOOP('',(#3221));
#1011=EDGE_LOOP('',(#3222));
#1012=EDGE_LOOP('',(#3223));
#1013=EDGE_LOOP('',(#3224));
#1339=LINE('',#6770,#1666);
#1340=LINE('',#6776,#1667);
#1666=VECTOR('',#5494,0.425);
#1667=VECTOR('',#5501,0.645);
#1957=CIRCLE('',#4783,0.425);
#1958=CIRCLE('',#4784,0.425);
#1959=CIRCLE('',#4786,0.645);
#1960=CIRCLE('',#4787,0.645);
#2156=VERTEX_POINT('',#6767);
#2157=VERTEX_POINT('',#6769);
#2158=VERTEX_POINT('',#6773);
#2159=VERTEX_POINT('',#6775);
#2555=EDGE_CURVE('',#2156,#2156,#1957,.T.);
#2556=EDGE_CURVE('',#2156,#2157,#1339,.T.);
#2557=EDGE_CURVE('',#2157,#2157,#1958,.T.);
#2558=EDGE_CURVE('',#2158,#2158,#1959,.T.);
#2559=EDGE_CURVE('',#2158,#2159,#1340,.T.);
#2560=EDGE_CURVE('',#2159,#2159,#1960,.T.);
#3213=ORIENTED_EDGE('',*,*,#2555,.F.);
#3214=ORIENTED_EDGE('',*,*,#2556,.T.);
#3215=ORIENTED_EDGE('',*,*,#2557,.T.);
#3216=ORIENTED_EDGE('',*,*,#2556,.F.);
#3217=ORIENTED_EDGE('',*,*,#2558,.F.);
#3218=ORIENTED_EDGE('',*,*,#2559,.T.);
#3219=ORIENTED_EDGE('',*,*,#2560,.T.);
#3220=ORIENTED_EDGE('',*,*,#2559,.F.);
#3221=ORIENTED_EDGE('',*,*,#2558,.T.);
#3222=ORIENTED_EDGE('',*,*,#2555,.T.);
#3223=ORIENTED_EDGE('',*,*,#2560,.F.);
#3224=ORIENTED_EDGE('',*,*,#2557,.F.);
#4025=CYLINDRICAL_SURFACE('',#4782,0.425);
#4026=CYLINDRICAL_SURFACE('',#4785,0.645);
#4140=ADVANCED_FACE('',(#722),#4025,.F.);
#4141=ADVANCED_FACE('',(#723),#4026,.T.);
#4142=ADVANCED_FACE('',(#724,#425),#532,.T.);
#4143=ADVANCED_FACE('',(#725,#426),#533,.F.);
#4334=CLOSED_SHELL('',(#4140,#4141,#4142,#4143));
#4781=AXIS2_PLACEMENT_3D('',#6765,#5488,#5489);
#4782=AXIS2_PLACEMENT_3D('',#6766,#5490,#5491);
#4783=AXIS2_PLACEMENT_3D('',#6768,#5492,#5493);
#4784=AXIS2_PLACEMENT_3D('',#6771,#5495,#5496);
#4785=AXIS2_PLACEMENT_3D('',#6772,#5497,#5498);
#4786=AXIS2_PLACEMENT_3D('',#6774,#5499,#5500);
#4787=AXIS2_PLACEMENT_3D('',#6777,#5502,#5503);
#4788=AXIS2_PLACEMENT_3D('',#6778,#5504,#5505);
#4789=AXIS2_PLACEMENT_3D('',#6779,#5506,#5507);
#5488=DIRECTION('axis',(0.,0.,1.));
#5489=DIRECTION('refdir',(1.,0.,0.));
#5490=DIRECTION('center_axis',(0.,0.,1.));
#5491=DIRECTION('ref_axis',(1.,0.,0.));
#5492=DIRECTION('center_axis',(0.,0.,-1.));
#5493=DIRECTION('ref_axis',(1.,0.,0.));
#5494=DIRECTION('',(0.,0.,-1.));
#5495=DIRECTION('center_axis',(0.,0.,-1.));
#5496=DIRECTION('ref_axis',(1.,0.,0.));
#5497=DIRECTION('center_axis',(0.,0.,1.));
#5498=DIRECTION('ref_axis',(1.,0.,0.));
#5499=DIRECTION('center_axis',(0.,0.,1.));
#5500=DIRECTION('ref_axis',(1.,0.,0.));
#5501=DIRECTION('',(0.,0.,-1.));
#5502=DIRECTION('center_axis',(0.,0.,1.));
#5503=DIRECTION('ref_axis',(1.,0.,0.));
#5504=DIRECTION('center_axis',(0.,0.,1.));
#5505=DIRECTION('ref_axis',(1.,0.,0.));
#5506=DIRECTION('center_axis',(0.,0.,1.));
#5507=DIRECTION('ref_axis',(1.,0.,0.));
#6765=CARTESIAN_POINT('',(0.,0.,0.));
#6766=CARTESIAN_POINT('Origin',(4.75,30.,1.2));
#6767=CARTESIAN_POINT('',(4.325,30.,2.4));
#6768=CARTESIAN_POINT('Origin',(4.75,30.,2.4));
#6769=CARTESIAN_POINT('',(4.325,30.,1.2));
#6770=CARTESIAN_POINT('',(4.325,30.,1.2));
#6771=CARTESIAN_POINT('Origin',(4.75,30.,1.2));
#6772=CARTESIAN_POINT('Origin',(4.75,30.,1.2));
#6773=CARTESIAN_POINT('',(4.105,30.,2.4));
#6774=CARTESIAN_POINT('Origin',(4.75,30.,2.4));
#6775=CARTESIAN_POINT('',(4.105,30.,1.2));
#6776=CARTESIAN_POINT('',(4.105,30.,1.2));
#6777=CARTESIAN_POINT('Origin',(4.75,30.,1.2));
#6778=CARTESIAN_POINT('Origin',(4.75,30.,2.4));
#6779=CARTESIAN_POINT('Origin',(4.75,30.,1.2));
#8326=UNCERTAINTY_MEASURE_WITH_UNIT(LENGTH_MEASURE(0.001),#8378,
'DISTANCE_ACCURACY_VALUE',
'Maximum model space distance between geometric entities at asserted c
onnectivities');
#8345=UNCERTAINTY_MEASURE_WITH_UNIT(LENGTH_MEASURE(0.001),#8378,
'DISTANCE_ACCURACY_VALUE',
'Maximum model space distance between geometric entities at asserted c
onnectivities');
#8358=(
GEOMETRIC_REPRESENTATION_CONTEXT(3)
GLOBAL_UNCERTAINTY_ASSIGNED_CONTEXT((#8326))
GLOBAL_UNIT_ASSIGNED_CONTEXT((#8378,#8380,#8381))
REPRESENTATION_CONTEXT('','3D')
);
#8377=(
GEOMETRIC_REPRESENTATION_CONTEXT(3)
GLOBAL_UNCERTAINTY_ASSIGNED_CONTEXT((#8345))
GLOBAL_UNIT_ASSIGNED_CONTEXT((#8378,#8380,#8381))
REPRESENTATION_CONTEXT('','3D')
);
#8378=(
LENGTH_UNIT()
NAMED_UNIT(*)
SI_UNIT(.CENTI.,.METRE.)
);
#8380=(
NAMED_UNIT(*)
PLANE_ANGLE_UNIT()
SI_UNIT($,.RADIAN.)
);
#8381=(
NAMED_UNIT(*)
SI_UNIT($,.STERADIAN.)
SOLID_ANGLE_UNIT()
);
#8394=SHAPE_DEFINITION_REPRESENTATION(#8425,#8509);
#8425=PRODUCT_DEFINITION_SHAPE('',$,#8541);
#8509=SHAPE_REPRESENTATION('',(#4781),#8358);
#8528=PRODUCT_DEFINITION_CONTEXT('part definition',#8623,'design');
#8541=PRODUCT_DEFINITION('Mounting reducer bush (5)',
'Mounting reducer bush (5)',#8572,#8528);
#8572=PRODUCT_DEFINITION_FORMATION('',$,#8637);
#8623=APPLICATION_CONTEXT(
'Core Data for Automotive Mechanical Design Process');
#8624=PRODUCT_CONTEXT('part definition',#8623,'mechanical');
#8637=PRODUCT('Mounting reducer bush (5)','Mounting reducer bush (5)',
'Mounting reducer bush (5)',(#8624));
#8726=COLOUR_RGB('Off White',0.89,0.88,0.83);
#8727=FILL_AREA_STYLE_COLOUR('',#8726);
#8728=FILL_AREA_STYLE('',(#8727));
#8729=SURFACE_STYLE_FILL_AREA(#8728);
#8730=SURFACE_SIDE_STYLE('',(#8729));
#8731=SURFACE_STYLE_USAGE(.BOTH.,#8730);
#8732=PRESENTATION_STYLE_ASSIGNMENT((#8731));
ENDSEC;
END-ISO-10303-21;
